ISO-10303-21;
HEADER;
/* Generated by software containing ST-Developer
 * from STEP Tools, Inc. (www.steptools.com) 
 */

FILE_DESCRIPTION(
/* description */ (''),
/* implementation_level */ '2;1');

FILE_NAME(
/* name */ 'M3_Nut_02 (1).step',
/* time_stamp */ '2026-10-22T15:07:41+06:00',
/* author */ (''),
/* organization */ (''),
/* preprocessor_version */ 'ST-DEVELOPER v20.2',
/* originating_system */ 'Autodesk Translation Framework v15.15.0.0',
/* authorisation */ '');

FILE_SCHEMA (('AUTOMOTIVE_DESIGN { 1 0 10303 214 3 1 1 }'));
ENDSEC;

DATA;
#10=MECHANICAL_DESIGN_GEOMETRIC_PRESENTATION_REPRESENTATION('',(#2888),#19220);
#77=SHAPE_REPRESENTATION_RELATIONSHIP('SRR','None',#19280,#91);
#91=ADVANCED_BREP_SHAPE_REPRESENTATION('',(#105),#19216);
#105=MANIFOLD_SOLID_BREP('M3_Nut_02',#11324);
#618=FACE_BOUND('',#4432,.T.);
#619=FACE_BOUND('',#4434,.T.);
#789=PLANE('',#12607);
#790=PLANE('',#12608);
#791=PLANE('',#12609);
#792=PLANE('',#12610);
#793=PLANE('',#12611);
#794=PLANE('',#12612);
#795=PLANE('',#12613);
#796=PLANE('',#12614);
#1549=LINE('',#18802,#2404);
#1550=LINE('',#18807,#2405);
#1551=LINE('',#18809,#2406);
#1552=LINE('',#18811,#2407);
#1553=LINE('',#18812,#2408);
#1554=LINE('',#18815,#2409);
#1555=LINE('',#18817,#2410);
#1556=LINE('',#18818,#2411);
#1557=LINE('',#18821,#2412);
#1558=LINE('',#18823,#2413);
#1559=LINE('',#18824,#2414);
#1560=LINE('',#18827,#2415);
#1561=LINE('',#18829,#2416);
#1562=LINE('',#18830,#2417);
#1563=LINE('',#18833,#2418);
#1564=LINE('',#18835,#2419);
#1565=LINE('',#18836,#2420);
#1566=LINE('',#18838,#2421);
#1567=LINE('',#18839,#2422);
#2404=VECTOR('',#15684,1.49999999999999);
#2405=VECTOR('',#15689,10.);
#2406=VECTOR('',#15690,10.);
#2407=VECTOR('',#15691,10.);
#2408=VECTOR('',#15692,10.);
#2409=VECTOR('',#15695,10.);
#2410=VECTOR('',#15696,10.);
#2411=VECTOR('',#15697,10.);
#2412=VECTOR('',#15700,10.);
#2413=VECTOR('',#15701,10.);
#2414=VECTOR('',#15702,10.);
#2415=VECTOR('',#15705,10.);
#2416=VECTOR('',#15706,10.);
#2417=VECTOR('',#15707,10.);
#2418=VECTOR('',#15710,10.);
#2419=VECTOR('',#15711,10.);
#2420=VECTOR('',#15712,10.);
#2421=VECTOR('',#15715,10.);
#2422=VECTOR('',#15716,10.);
#2857=CYLINDRICAL_SURFACE('',#12604,1.465);
#2888=STYLED_ITEM('',(#19410),#105);
#3369=FACE_OUTER_BOUND('',#4424,.T.);
#3370=FACE_OUTER_BOUND('',#4425,.T.);
#3371=FACE_OUTER_BOUND('',#4426,.T.);
#3372=FACE_OUTER_BOUND('',#4427,.T.);
#3373=FACE_OUTER_BOUND('',#4428,.T.);
#3374=FACE_OUTER_BOUND('',#4429,.T.);
#3375=FACE_OUTER_BOUND('',#4430,.T.);
#3376=FACE_OUTER_BOUND('',#4431,.T.);
#3377=FACE_OUTER_BOUND('',#4433,.T.);
#4424=EDGE_LOOP('',(#10396,#10397,#10398,#10399));
#4425=EDGE_LOOP('',(#10400,#10401,#10402,#10403));
#4426=EDGE_LOOP('',(#10404,#10405,#10406,#10407));
#4427=EDGE_LOOP('',(#10408,#10409,#10410,#10411));
#4428=EDGE_LOOP('',(#10412,#10413,#10414,#10415));
#4429=EDGE_LOOP('',(#10416,#10417,#10418,#10419));
#4430=EDGE_LOOP('',(#10420,#10421,#10422,#10423));
#4431=EDGE_LOOP('',(#10424,#10425,#10426,#10427,#10428,#10429));
#4432=EDGE_LOOP('',(#10430));
#4433=EDGE_LOOP('',(#10431,#10432,#10433,#10434,#10435,#10436));
#4434=EDGE_LOOP('',(#10437));
#5133=CIRCLE('',#12605,1.465);
#5134=CIRCLE('',#12606,1.465);
#6065=VERTEX_POINT('',#18799);
#6066=VERTEX_POINT('',#18801);
#6067=VERTEX_POINT('',#18805);
#6068=VERTEX_POINT('',#18806);
#6069=VERTEX_POINT('',#18808);
#6070=VERTEX_POINT('',#18810);
#6071=VERTEX_POINT('',#18814);
#6072=VERTEX_POINT('',#18816);
#6073=VERTEX_POINT('',#18820);
#6074=VERTEX_POINT('',#18822);
#6075=VERTEX_POINT('',#18826);
#6076=VERTEX_POINT('',#18828);
#6077=VERTEX_POINT('',#18832);
#6078=VERTEX_POINT('',#18834);
#7529=EDGE_CURVE('',#6065,#6065,#5133,.T.);
#7530=EDGE_CURVE('',#6065,#6066,#1549,.T.);
#7531=EDGE_CURVE('',#6066,#6066,#5134,.F.);
#7532=EDGE_CURVE('',#6067,#6068,#1550,.T.);
#7533=EDGE_CURVE('',#6067,#6069,#1551,.T.);
#7534=EDGE_CURVE('',#6070,#6069,#1552,.T.);
#7535=EDGE_CURVE('',#6068,#6070,#1553,.T.);
#7536=EDGE_CURVE('',#6068,#6071,#1554,.T.);
#7537=EDGE_CURVE('',#6072,#6070,#1555,.T.);
#7538=EDGE_CURVE('',#6071,#6072,#1556,.T.);
#7539=EDGE_CURVE('',#6071,#6073,#1557,.T.);
#7540=EDGE_CURVE('',#6074,#6072,#1558,.T.);
#7541=EDGE_CURVE('',#6073,#6074,#1559,.T.);
#7542=EDGE_CURVE('',#6073,#6075,#1560,.T.);
#7543=EDGE_CURVE('',#6076,#6074,#1561,.T.);
#7544=EDGE_CURVE('',#6075,#6076,#1562,.T.);
#7545=EDGE_CURVE('',#6075,#6077,#1563,.T.);
#7546=EDGE_CURVE('',#6078,#6076,#1564,.T.);
#7547=EDGE_CURVE('',#6077,#6078,#1565,.T.);
#7548=EDGE_CURVE('',#6077,#6067,#1566,.T.);
#7549=EDGE_CURVE('',#6069,#6078,#1567,.T.);
#10396=ORIENTED_EDGE('',*,*,#7529,.F.);
#10397=ORIENTED_EDGE('',*,*,#7530,.T.);
#10398=ORIENTED_EDGE('',*,*,#7531,.F.);
#10399=ORIENTED_EDGE('',*,*,#7530,.F.);
#10400=ORIENTED_EDGE('',*,*,#7532,.F.);
#10401=ORIENTED_EDGE('',*,*,#7533,.T.);
#10402=ORIENTED_EDGE('',*,*,#7534,.F.);
#10403=ORIENTED_EDGE('',*,*,#7535,.F.);
#10404=ORIENTED_EDGE('',*,*,#7536,.F.);
#10405=ORIENTED_EDGE('',*,*,#7535,.T.);
#10406=ORIENTED_EDGE('',*,*,#7537,.F.);
#10407=ORIENTED_EDGE('',*,*,#7538,.F.);
#10408=ORIENTED_EDGE('',*,*,#7539,.F.);
#10409=ORIENTED_EDGE('',*,*,#7538,.T.);
#10410=ORIENTED_EDGE('',*,*,#7540,.F.);
#10411=ORIENTED_EDGE('',*,*,#7541,.F.);
#10412=ORIENTED_EDGE('',*,*,#7542,.F.);
#10413=ORIENTED_EDGE('',*,*,#7541,.T.);
#10414=ORIENTED_EDGE('',*,*,#7543,.F.);
#10415=ORIENTED_EDGE('',*,*,#7544,.F.);
#10416=ORIENTED_EDGE('',*,*,#7545,.F.);
#10417=ORIENTED_EDGE('',*,*,#7544,.T.);
#10418=ORIENTED_EDGE('',*,*,#7546,.F.);
#10419=ORIENTED_EDGE('',*,*,#7547,.F.);
#10420=ORIENTED_EDGE('',*,*,#7548,.F.);
#10421=ORIENTED_EDGE('',*,*,#7547,.T.);
#10422=ORIENTED_EDGE('',*,*,#7549,.F.);
#10423=ORIENTED_EDGE('',*,*,#7533,.F.);
#10424=ORIENTED_EDGE('',*,*,#7548,.T.);
#10425=ORIENTED_EDGE('',*,*,#7532,.T.);
#10426=ORIENTED_EDGE('',*,*,#7536,.T.);
#10427=ORIENTED_EDGE('',*,*,#7539,.T.);
#10428=ORIENTED_EDGE('',*,*,#7542,.T.);
#10429=ORIENTED_EDGE('',*,*,#7545,.T.);
#10430=ORIENTED_EDGE('',*,*,#7531,.T.);
#10431=ORIENTED_EDGE('',*,*,#7549,.T.);
#10432=ORIENTED_EDGE('',*,*,#7546,.T.);
#10433=ORIENTED_EDGE('',*,*,#7543,.T.);
#10434=ORIENTED_EDGE('',*,*,#7540,.T.);
#10435=ORIENTED_EDGE('',*,*,#7537,.T.);
#10436=ORIENTED_EDGE('',*,*,#7534,.T.);
#10437=ORIENTED_EDGE('',*,*,#7529,.T.);
#11245=ADVANCED_FACE('',(#3369),#2857,.F.);
#11246=ADVANCED_FACE('',(#3370),#789,.T.);
#11247=ADVANCED_FACE('',(#3371),#790,.T.);
#11248=ADVANCED_FACE('',(#3372),#791,.T.);
#11249=ADVANCED_FACE('',(#3373),#792,.T.);
#11250=ADVANCED_FACE('',(#3374),#793,.T.);
#11251=ADVANCED_FACE('',(#3375),#794,.T.);
#11252=ADVANCED_FACE('',(#3376,#618),#795,.T.);
#11253=ADVANCED_FACE('',(#3377,#619),#796,.F.);
#11324=CLOSED_SHELL('',(#11245,#11246,#11247,#11248,#11249,#11250,#11251,
#11252,#11253));
#12603=AXIS2_PLACEMENT_3D('',#18797,#15678,#15679);
#12604=AXIS2_PLACEMENT_3D('',#18798,#15680,#15681);
#12605=AXIS2_PLACEMENT_3D('',#18800,#15682,#15683);
#12606=AXIS2_PLACEMENT_3D('',#18803,#15685,#15686);
#12607=AXIS2_PLACEMENT_3D('',#18804,#15687,#15688);
#12608=AXIS2_PLACEMENT_3D('',#18813,#15693,#15694);
#12609=AXIS2_PLACEMENT_3D('',#18819,#15698,#15699);
#12610=AXIS2_PLACEMENT_3D('',#18825,#15703,#15704);
#12611=AXIS2_PLACEMENT_3D('',#18831,#15708,#15709);
#12612=AXIS2_PLACEMENT_3D('',#18837,#15713,#15714);
#12613=AXIS2_PLACEMENT_3D('',#18840,#15717,#15718);
#12614=AXIS2_PLACEMENT_3D('',#18841,#15719,#15720);
#15678=DIRECTION('axis',(0.,0.,1.));
#15679=DIRECTION('refdir',(1.,0.,0.));
#15680=DIRECTION('center_axis',(0.,-1.,0.));
#15681=DIRECTION('ref_axis',(-1.,0.,0.));
#15682=DIRECTION('center_axis',(0.,1.,0.));
#15683=DIRECTION('ref_axis',(-1.,0.,0.));
#15684=DIRECTION('',(0.,1.,0.));
#15685=DIRECTION('center_axis',(0.,1.,0.));
#15686=DIRECTION('ref_axis',(-1.,0.,0.));
#15687=DIRECTION('center_axis',(-0.866025403784439,0.,-0.499999999999999));
#15688=DIRECTION('ref_axis',(0.499999999999999,0.,-0.866025403784439));
#15689=DIRECTION('',(-0.499999999999999,0.,0.866025403784439));
#15690=DIRECTION('',(0.,-1.,0.));
#15691=DIRECTION('',(0.499999999999999,0.,-0.866025403784439));
#15692=DIRECTION('',(0.,-1.,0.));
#15693=DIRECTION('center_axis',(-0.866025403784439,0.,0.499999999999999));
#15694=DIRECTION('ref_axis',(-0.499999999999999,0.,-0.866025403784439));
#15695=DIRECTION('',(0.499999999999999,0.,0.866025403784439));
#15696=DIRECTION('',(-0.499999999999999,0.,-0.866025403784439));
#15697=DIRECTION('',(0.,-1.,0.));
#15698=DIRECTION('center_axis',(0.,0.,1.));
#15699=DIRECTION('ref_axis',(-1.,0.,0.));
#15700=DIRECTION('',(1.,0.,0.));
#15701=DIRECTION('',(-1.,0.,0.));
#15702=DIRECTION('',(0.,-1.,0.));
#15703=DIRECTION('center_axis',(0.866025403784438,0.,0.500000000000001));
#15704=DIRECTION('ref_axis',(-0.500000000000001,0.,0.866025403784438));
#15705=DIRECTION('',(0.500000000000001,0.,-0.866025403784438));
#15706=DIRECTION('',(-0.500000000000001,0.,0.866025403784438));
#15707=DIRECTION('',(0.,-1.,0.));
#15708=DIRECTION('center_axis',(0.866025403784439,0.,-0.5));
#15709=DIRECTION('ref_axis',(0.5,0.,0.866025403784439));
#15710=DIRECTION('',(-0.5,0.,-0.866025403784439));
#15711=DIRECTION('',(0.5,0.,0.866025403784439));
#15712=DIRECTION('',(0.,-1.,0.));
#15713=DIRECTION('center_axis',(4.61511044732058E-15,0.,-1.));
#15714=DIRECTION('ref_axis',(1.,0.,4.61511044732058E-15));
#15715=DIRECTION('',(-1.,0.,-4.61511044732058E-15));
#15716=DIRECTION('',(1.,0.,4.61511044732058E-15));
#15717=DIRECTION('center_axis',(0.,1.,0.));
#15718=DIRECTION('ref_axis',(-1.,0.,0.));
#15719=DIRECTION('center_axis',(0.,1.,0.));
#15720=DIRECTION('ref_axis',(-1.,0.,0.));
#18797=CARTESIAN_POINT('',(0.,0.,0.));
#18798=CARTESIAN_POINT('Origin',(363.987734179926,58.5,25.7372649179816));
#18799=CARTESIAN_POINT('',(365.452734179926,56.5,25.7372649179816));
#18800=CARTESIAN_POINT('Origin',(363.987734179926,56.5,25.7372649179816));
#18801=CARTESIAN_POINT('',(365.452734179926,58.5,25.7372649179816));
#18802=CARTESIAN_POINT('',(365.452734179926,58.5,25.7372649179816));
#18803=CARTESIAN_POINT('Origin',(363.987734179926,58.5,25.7372649179816));
#18804=CARTESIAN_POINT('Origin',(361.100982833978,58.5,25.7372649179816));
#18805=CARTESIAN_POINT('',(362.544358506952,58.5,23.2372649179816));
#18806=CARTESIAN_POINT('',(361.100982833978,58.5,25.7372649179816));
#18807=CARTESIAN_POINT('',(362.544358506952,58.5,23.2372649179816));
#18808=CARTESIAN_POINT('',(362.544358506952,56.5,23.2372649179816));
#18809=CARTESIAN_POINT('',(362.544358506952,58.5,23.2372649179816));
#18810=CARTESIAN_POINT('',(361.100982833978,56.5,25.7372649179816));
#18811=CARTESIAN_POINT('',(362.544358506952,56.5,23.2372649179816));
#18812=CARTESIAN_POINT('',(361.100982833978,58.5,25.7372649179816));
#18813=CARTESIAN_POINT('Origin',(362.544358506952,58.5,28.2372649179815));
#18814=CARTESIAN_POINT('',(362.544358506952,58.5,28.2372649179815));
#18815=CARTESIAN_POINT('',(361.100982833978,58.5,25.7372649179816));
#18816=CARTESIAN_POINT('',(362.544358506952,56.5,28.2372649179815));
#18817=CARTESIAN_POINT('',(361.100982833978,56.5,25.7372649179816));
#18818=CARTESIAN_POINT('',(362.544358506952,58.5,28.2372649179815));
#18819=CARTESIAN_POINT('Origin',(365.4311098529,58.5,28.2372649179815));
#18820=CARTESIAN_POINT('',(365.4311098529,58.5,28.2372649179815));
#18821=CARTESIAN_POINT('',(362.544358506952,58.5,28.2372649179815));
#18822=CARTESIAN_POINT('',(365.4311098529,56.5,28.2372649179815));
#18823=CARTESIAN_POINT('',(362.544358506952,56.5,28.2372649179815));
#18824=CARTESIAN_POINT('',(365.4311098529,58.5,28.2372649179815));
#18825=CARTESIAN_POINT('Origin',(366.874485525875,58.5,25.7372649179816));
#18826=CARTESIAN_POINT('',(366.874485525875,58.5,25.7372649179816));
#18827=CARTESIAN_POINT('',(365.4311098529,58.5,28.2372649179815));
#18828=CARTESIAN_POINT('',(366.874485525875,56.5,25.7372649179816));
#18829=CARTESIAN_POINT('',(365.4311098529,56.5,28.2372649179815));
#18830=CARTESIAN_POINT('',(366.874485525875,58.5,25.7372649179816));
#18831=CARTESIAN_POINT('Origin',(365.4311098529,58.5,23.2372649179816));
#18832=CARTESIAN_POINT('',(365.4311098529,58.5,23.2372649179816));
#18833=CARTESIAN_POINT('',(366.874485525875,58.5,25.7372649179816));
#18834=CARTESIAN_POINT('',(365.4311098529,56.5,23.2372649179816));
#18835=CARTESIAN_POINT('',(366.874485525875,56.5,25.7372649179816));
#18836=CARTESIAN_POINT('',(365.4311098529,58.5,23.2372649179816));
#18837=CARTESIAN_POINT('Origin',(362.544358506952,58.5,23.2372649179816));
#18838=CARTESIAN_POINT('',(365.4311098529,58.5,23.2372649179816));
#18839=CARTESIAN_POINT('',(365.4311098529,56.5,23.2372649179816));
#18840=CARTESIAN_POINT('Origin',(363.987734179926,58.5,25.7372649179816));
#18841=CARTESIAN_POINT('Origin',(363.987734179926,56.5,25.7372649179816));
#19200=UNCERTAINTY_MEASURE_WITH_UNIT(LENGTH_MEASURE(0.01),#19221,
'DISTANCE_ACCURACY_VALUE',
'Maximum model space distance between geometric entities at asserted c
onnectivities');
#19204=UNCERTAINTY_MEASURE_WITH_UNIT(LENGTH_MEASURE(0.01),#19221,
'DISTANCE_ACCURACY_VALUE',
'Maximum model space distance between geometric entities at asserted c
onnectivities');
#19216=(
GEOMETRIC_REPRESENTATION_CONTEXT(3)
GLOBAL_UNCERTAINTY_ASSIGNED_CONTEXT((#19200))
GLOBAL_UNIT_ASSIGNED_CONTEXT((#19221,#19223,#19224))
REPRESENTATION_CONTEXT('','3D')
);
#19220=(
GEOMETRIC_REPRESENTATION_CONTEXT(3)
GLOBAL_UNCERTAINTY_ASSIGNED_CONTEXT((#19204))
GLOBAL_UNIT_ASSIGNED_CONTEXT((#19221,#19223,#19224))
REPRESENTATION_CONTEXT('','3D')
);
#19221=(
LENGTH_UNIT()
NAMED_UNIT(*)
SI_UNIT(.MILLI.,.METRE.)
);
#19223=(
NAMED_UNIT(*)
PLANE_ANGLE_UNIT()
SI_UNIT($,.RADIAN.)
);
#19224=(
NAMED_UNIT(*)
SI_UNIT($,.STERADIAN.)
SOLID_ANGLE_UNIT()
);
#19236=SHAPE_DEFINITION_REPRESENTATION(#19251,#19280);
#19251=PRODUCT_DEFINITION_SHAPE('',$,#19296);
#19280=SHAPE_REPRESENTATION('',(#12603),#19216);
#19284=PRODUCT_DEFINITION_CONTEXT('part definition',#19331,'design');
#19296=PRODUCT_DEFINITION('M3_Nut_02 (1)','M3_Nut_02 (1)',#19311,#19284);
#19311=PRODUCT_DEFINITION_FORMATION('',$,#19344);
#19331=APPLICATION_CONTEXT(
'Core Data for Automotive Mechanical Design Process');
#19332=PRODUCT_CONTEXT('part definition',#19331,'mechanical');
#19344=PRODUCT('M3_Nut_02 (1)','M3_Nut_02 (1)',$,(#19332));
#19404=COLOUR_RGB('Black',0.12,0.14,0.17);
#19405=FILL_AREA_STYLE_COLOUR('',#19404);
#19406=FILL_AREA_STYLE('',(#19405));
#19407=SURFACE_STYLE_FILL_AREA(#19406);
#19408=SURFACE_SIDE_STYLE('',(#19407));
#19409=SURFACE_STYLE_USAGE(.BOTH.,#19408);
#19410=PRESENTATION_STYLE_ASSIGNMENT((#19409));
ENDSEC;
END-ISO-10303-21;
